ISO-10303-21;
HEADER;
/* Generated by software containing ST-Developer
 * from STEP Tools, Inc. (www.steptools.com) 
 */

FILE_DESCRIPTION(
/* description */ ('Worm-less right-angle friction wheel drive'),
/* implementation_level */ '2;1');

FILE_NAME(
/* name */ 'M4x10 Cap Screw.step',
/* time_stamp */ '2026-10-28T03:22:36-07:00',
/* author */ (''),
/* organization */ (''),
/* preprocessor_version */ 'ST-DEVELOPER v20.2',
/* originating_system */ 'Autodesk Translation Framework v15.17.0.0',
/* authorisation */ '');

FILE_SCHEMA (('AUTOMOTIVE_DESIGN { 1 0 10303 214 3 1 1 }'));
ENDSEC;

DATA;
#10=MECHANICAL_DESIGN_GEOMETRIC_PRESENTATION_REPRESENTATION('',(#647),#17046);
#452=ORIENTED_CLOSED_SHELL('',*,#8203,.F.);
#463=CONICAL_SURFACE('',#9402,0.325,0.785398163397448);
#464=CONICAL_SURFACE('',#9406,0.335,0.785398163397448);
#465=CONICAL_SURFACE('',#9410,0.21,0.463647609000806);
#478=BREP_WITH_VOIDS('Body1',#8204,(#452));
#546=SHAPE_REPRESENTATION_RELATIONSHIP('SRR','None',#17290,#593);
#593=ADVANCED_BREP_SHAPE_REPRESENTATION('',(#478),#17026);
#647=STYLED_ITEM('',(#17598),#478);
#915=FACE_BOUND('',#2187,.T.);
#1095=PLANE('',#9390);
#1096=PLANE('',#9391);
#1097=PLANE('',#9392);
#1098=PLANE('',#9393);
#1099=PLANE('',#9394);
#1100=PLANE('',#9395);
#1101=PLANE('',#9396);
#1102=PLANE('',#9397);
#1103=PLANE('',#9398);
#1104=PLANE('',#9400);
#1105=PLANE('',#9408);
#1507=FACE_OUTER_BOUND('',#2173,.T.);
#1508=FACE_OUTER_BOUND('',#2174,.T.);
#1509=FACE_OUTER_BOUND('',#2175,.T.);
#1510=FACE_OUTER_BOUND('',#2176,.T.);
#1511=FACE_OUTER_BOUND('',#2177,.T.);
#1512=FACE_OUTER_BOUND('',#2178,.T.);
#1513=FACE_OUTER_BOUND('',#2179,.T.);
#1514=FACE_OUTER_BOUND('',#2180,.T.);
#1515=FACE_OUTER_BOUND('',#2181,.T.);
#1516=FACE_OUTER_BOUND('',#2182,.T.);
#1517=FACE_OUTER_BOUND('',#2183,.T.);
#1518=FACE_OUTER_BOUND('',#2184,.T.);
#1519=FACE_OUTER_BOUND('',#2185,.T.);
#1520=FACE_OUTER_BOUND('',#2186,.T.);
#1521=FACE_OUTER_BOUND('',#2188,.T.);
#1522=FACE_OUTER_BOUND('',#2189,.T.);
#2173=EDGE_LOOP('',(#6864,#6865,#6866,#6867));
#2174=EDGE_LOOP('',(#6868,#6869,#6870,#6871));
#2175=EDGE_LOOP('',(#6872,#6873,#6874,#6875));
#2176=EDGE_LOOP('',(#6876,#6877,#6878,#6879));
#2177=EDGE_LOOP('',(#6880,#6881,#6882,#6883));
#2178=EDGE_LOOP('',(#6884,#6885,#6886,#6887));
#2179=EDGE_LOOP('',(#6888,#6889,#6890,#6891,#6892,#6893));
#2180=EDGE_LOOP('',(#6894,#6895,#6896,#6897,#6898,#6899));
#2181=EDGE_LOOP('',(#6900));
#2182=EDGE_LOOP('',(#6901));
#2183=EDGE_LOOP('',(#6902,#6903,#6904,#6905));
#2184=EDGE_LOOP('',(#6906,#6907,#6908,#6909));
#2185=EDGE_LOOP('',(#6910,#6911,#6912,#6913));
#2186=EDGE_LOOP('',(#6914));
#2187=EDGE_LOOP('',(#6915));
#2188=EDGE_LOOP('',(#6916,#6917,#6918,#6919));
#2189=EDGE_LOOP('',(#6920,#6921,#6922,#6923));
#2713=LINE('',#15924,#3253);
#2714=LINE('',#15926,#3254);
#2715=LINE('',#15928,#3255);
#2716=LINE('',#15929,#3256);
#2717=LINE('',#15932,#3257);
#2718=LINE('',#15934,#3258);
#2719=LINE('',#15935,#3259);
#2720=LINE('',#15938,#3260);
#2721=LINE('',#15940,#3261);
#2722=LINE('',#15941,#3262);
#2723=LINE('',#15944,#3263);
#2724=LINE('',#15946,#3264);
#2725=LINE('',#15947,#3265);
#2726=LINE('',#15950,#3266);
#2727=LINE('',#15952,#3267);
#2728=LINE('',#15953,#3268);
#2729=LINE('',#15955,#3269);
#2730=LINE('',#15956,#3270);
#2731=LINE('',#15968,#3271);
#2732=LINE('',#15972,#3272);
#2733=LINE('',#15976,#3273);
#2734=LINE('',#15983,#3274);
#2735=LINE('',#15985,#3275);
#3253=VECTOR('',#11407,1.);
#3254=VECTOR('',#11408,1.);
#3255=VECTOR('',#11409,1.);
#3256=VECTOR('',#11410,1.);
#3257=VECTOR('',#11413,1.);
#3258=VECTOR('',#11414,1.);
#3259=VECTOR('',#11415,1.);
#3260=VECTOR('',#11418,1.);
#3261=VECTOR('',#11419,1.);
#3262=VECTOR('',#11420,1.);
#3263=VECTOR('',#11423,1.);
#3264=VECTOR('',#11424,1.);
#3265=VECTOR('',#11425,1.);
#3266=VECTOR('',#11428,1.);
#3267=VECTOR('',#11429,1.);
#3268=VECTOR('',#11430,1.);
#3269=VECTOR('',#11433,1.);
#3270=VECTOR('',#11434,1.);
#3271=VECTOR('',#11451,0.325);
#3272=VECTOR('',#11456,0.35);
#3273=VECTOR('',#11461,0.335);
#3274=VECTOR('',#11470,0.21);
#3275=VECTOR('',#11473,0.2);
#3770=CIRCLE('',#9399,0.1954);
#3771=CIRCLE('',#9401,0.3);
#3772=CIRCLE('',#9403,0.35);
#3773=CIRCLE('',#9405,0.35);
#3774=CIRCLE('',#9407,0.32);
#3775=CIRCLE('',#9409,0.22);
#3776=CIRCLE('',#9411,0.1954);
#4319=VERTEX_POINT('',#15922);
#4320=VERTEX_POINT('',#15923);
#4321=VERTEX_POINT('',#15925);
#4322=VERTEX_POINT('',#15927);
#4323=VERTEX_POINT('',#15931);
#4324=VERTEX_POINT('',#15933);
#4325=VERTEX_POINT('',#15937);
#4326=VERTEX_POINT('',#15939);
#4327=VERTEX_POINT('',#15943);
#4328=VERTEX_POINT('',#15945);
#4329=VERTEX_POINT('',#15949);
#4330=VERTEX_POINT('',#15951);
#4331=VERTEX_POINT('',#15960);
#4332=VERTEX_POINT('',#15963);
#4333=VERTEX_POINT('',#15966);
#4334=VERTEX_POINT('',#15970);
#4335=VERTEX_POINT('',#15974);
#4336=VERTEX_POINT('',#15978);
#4337=VERTEX_POINT('',#15981);
#5201=EDGE_CURVE('',#4319,#4320,#2713,.T.);
#5202=EDGE_CURVE('',#4320,#4321,#2714,.T.);
#5203=EDGE_CURVE('',#4321,#4322,#2715,.T.);
#5204=EDGE_CURVE('',#4319,#4322,#2716,.T.);
#5205=EDGE_CURVE('',#4320,#4323,#2717,.T.);
#5206=EDGE_CURVE('',#4323,#4324,#2718,.T.);
#5207=EDGE_CURVE('',#4324,#4321,#2719,.T.);
#5208=EDGE_CURVE('',#4323,#4325,#2720,.T.);
#5209=EDGE_CURVE('',#4325,#4326,#2721,.T.);
#5210=EDGE_CURVE('',#4326,#4324,#2722,.T.);
#5211=EDGE_CURVE('',#4325,#4327,#2723,.T.);
#5212=EDGE_CURVE('',#4327,#4328,#2724,.T.);
#5213=EDGE_CURVE('',#4328,#4326,#2725,.T.);
#5214=EDGE_CURVE('',#4327,#4329,#2726,.T.);
#5215=EDGE_CURVE('',#4329,#4330,#2727,.T.);
#5216=EDGE_CURVE('',#4330,#4328,#2728,.T.);
#5217=EDGE_CURVE('',#4329,#4319,#2729,.T.);
#5218=EDGE_CURVE('',#4322,#4330,#2730,.T.);
#5219=EDGE_CURVE('',#4331,#4331,#3770,.T.);
#5220=EDGE_CURVE('',#4332,#4332,#3771,.T.);
#5221=EDGE_CURVE('',#4333,#4333,#3772,.T.);
#5222=EDGE_CURVE('',#4333,#4332,#2731,.T.);
#5223=EDGE_CURVE('',#4334,#4334,#3773,.T.);
#5224=EDGE_CURVE('',#4334,#4333,#2732,.T.);
#5225=EDGE_CURVE('',#4335,#4335,#3774,.T.);
#5226=EDGE_CURVE('',#4335,#4334,#2733,.T.);
#5227=EDGE_CURVE('',#4336,#4336,#3775,.T.);
#5228=EDGE_CURVE('',#4337,#4337,#3776,.F.);
#5229=EDGE_CURVE('',#4337,#4336,#2734,.T.);
#5230=EDGE_CURVE('',#4331,#4337,#2735,.T.);
#6864=ORIENTED_EDGE('',*,*,#5201,.T.);
#6865=ORIENTED_EDGE('',*,*,#5202,.T.);
#6866=ORIENTED_EDGE('',*,*,#5203,.T.);
#6867=ORIENTED_EDGE('',*,*,#5204,.F.);
#6868=ORIENTED_EDGE('',*,*,#5205,.T.);
#6869=ORIENTED_EDGE('',*,*,#5206,.T.);
#6870=ORIENTED_EDGE('',*,*,#5207,.T.);
#6871=ORIENTED_EDGE('',*,*,#5202,.F.);
#6872=ORIENTED_EDGE('',*,*,#5208,.T.);
#6873=ORIENTED_EDGE('',*,*,#5209,.T.);
#6874=ORIENTED_EDGE('',*,*,#5210,.T.);
#6875=ORIENTED_EDGE('',*,*,#5206,.F.);
#6876=ORIENTED_EDGE('',*,*,#5211,.T.);
#6877=ORIENTED_EDGE('',*,*,#5212,.T.);
#6878=ORIENTED_EDGE('',*,*,#5213,.T.);
#6879=ORIENTED_EDGE('',*,*,#5209,.F.);
#6880=ORIENTED_EDGE('',*,*,#5214,.T.);
#6881=ORIENTED_EDGE('',*,*,#5215,.T.);
#6882=ORIENTED_EDGE('',*,*,#5216,.T.);
#6883=ORIENTED_EDGE('',*,*,#5212,.F.);
#6884=ORIENTED_EDGE('',*,*,#5217,.T.);
#6885=ORIENTED_EDGE('',*,*,#5204,.T.);
#6886=ORIENTED_EDGE('',*,*,#5218,.T.);
#6887=ORIENTED_EDGE('',*,*,#5215,.F.);
#6888=ORIENTED_EDGE('',*,*,#5217,.F.);
#6889=ORIENTED_EDGE('',*,*,#5214,.F.);
#6890=ORIENTED_EDGE('',*,*,#5211,.F.);
#6891=ORIENTED_EDGE('',*,*,#5208,.F.);
#6892=ORIENTED_EDGE('',*,*,#5205,.F.);
#6893=ORIENTED_EDGE('',*,*,#5201,.F.);
#6894=ORIENTED_EDGE('',*,*,#5218,.F.);
#6895=ORIENTED_EDGE('',*,*,#5203,.F.);
#6896=ORIENTED_EDGE('',*,*,#5207,.F.);
#6897=ORIENTED_EDGE('',*,*,#5210,.F.);
#6898=ORIENTED_EDGE('',*,*,#5213,.F.);
#6899=ORIENTED_EDGE('',*,*,#5216,.F.);
#6900=ORIENTED_EDGE('',*,*,#5219,.F.);
#6901=ORIENTED_EDGE('',*,*,#5220,.F.);
#6902=ORIENTED_EDGE('',*,*,#5221,.F.);
#6903=ORIENTED_EDGE('',*,*,#5222,.T.);
#6904=ORIENTED_EDGE('',*,*,#5220,.T.);
#6905=ORIENTED_EDGE('',*,*,#5222,.F.);
#6906=ORIENTED_EDGE('',*,*,#5223,.F.);
#6907=ORIENTED_EDGE('',*,*,#5224,.T.);
#6908=ORIENTED_EDGE('',*,*,#5221,.T.);
#6909=ORIENTED_EDGE('',*,*,#5224,.F.);
#6910=ORIENTED_EDGE('',*,*,#5225,.F.);
#6911=ORIENTED_EDGE('',*,*,#5226,.T.);
#6912=ORIENTED_EDGE('',*,*,#5223,.T.);
#6913=ORIENTED_EDGE('',*,*,#5226,.F.);
#6914=ORIENTED_EDGE('',*,*,#5225,.T.);
#6915=ORIENTED_EDGE('',*,*,#5227,.F.);
#6916=ORIENTED_EDGE('',*,*,#5228,.F.);
#6917=ORIENTED_EDGE('',*,*,#5229,.T.);
#6918=ORIENTED_EDGE('',*,*,#5227,.T.);
#6919=ORIENTED_EDGE('',*,*,#5229,.F.);
#6920=ORIENTED_EDGE('',*,*,#5219,.T.);
#6921=ORIENTED_EDGE('',*,*,#5230,.T.);
#6922=ORIENTED_EDGE('',*,*,#5228,.T.);
#6923=ORIENTED_EDGE('',*,*,#5230,.F.);
#7660=CYLINDRICAL_SURFACE('',#9404,0.35);
#7661=CYLINDRICAL_SURFACE('',#9412,0.1954);
#7999=ADVANCED_FACE('',(#1507),#1095,.F.);
#8000=ADVANCED_FACE('',(#1508),#1096,.F.);
#8001=ADVANCED_FACE('',(#1509),#1097,.F.);
#8002=ADVANCED_FACE('',(#1510),#1098,.F.);
#8003=ADVANCED_FACE('',(#1511),#1099,.F.);
#8004=ADVANCED_FACE('',(#1512),#1100,.F.);
#8005=ADVANCED_FACE('',(#1513),#1101,.F.);
#8006=ADVANCED_FACE('',(#1514),#1102,.F.);
#8007=ADVANCED_FACE('',(#1515),#1103,.F.);
#8008=ADVANCED_FACE('',(#1516),#1104,.T.);
#8009=ADVANCED_FACE('',(#1517),#463,.T.);
#8010=ADVANCED_FACE('',(#1518),#7660,.T.);
#8011=ADVANCED_FACE('',(#1519),#464,.T.);
#8012=ADVANCED_FACE('',(#1520,#915),#1105,.T.);
#8013=ADVANCED_FACE('',(#1521),#465,.T.);
#8014=ADVANCED_FACE('',(#1522),#7661,.T.);
#8203=CLOSED_SHELL('',(#7999,#8000,#8001,#8002,#8003,#8004,#8005,#8006));
#8204=CLOSED_SHELL('',(#8007,#8008,#8009,#8010,#8011,#8012,#8013,#8014));
#9389=AXIS2_PLACEMENT_3D('',#15920,#11403,#11404);
#9390=AXIS2_PLACEMENT_3D('',#15921,#11405,#11406);
#9391=AXIS2_PLACEMENT_3D('',#15930,#11411,#11412);
#9392=AXIS2_PLACEMENT_3D('',#15936,#11416,#11417);
#9393=AXIS2_PLACEMENT_3D('',#15942,#11421,#11422);
#9394=AXIS2_PLACEMENT_3D('',#15948,#11426,#11427);
#9395=AXIS2_PLACEMENT_3D('',#15954,#11431,#11432);
#9396=AXIS2_PLACEMENT_3D('',#15957,#11435,#11436);
#9397=AXIS2_PLACEMENT_3D('',#15958,#11437,#11438);
#9398=AXIS2_PLACEMENT_3D('',#15959,#11439,#11440);
#9399=AXIS2_PLACEMENT_3D('',#15961,#11441,#11442);
#9400=AXIS2_PLACEMENT_3D('',#15962,#11443,#11444);
#9401=AXIS2_PLACEMENT_3D('',#15964,#11445,#11446);
#9402=AXIS2_PLACEMENT_3D('',#15965,#11447,#11448);
#9403=AXIS2_PLACEMENT_3D('',#15967,#11449,#11450);
#9404=AXIS2_PLACEMENT_3D('',#15969,#11452,#11453);
#9405=AXIS2_PLACEMENT_3D('',#15971,#11454,#11455);
#9406=AXIS2_PLACEMENT_3D('',#15973,#11457,#11458);
#9407=AXIS2_PLACEMENT_3D('',#15975,#11459,#11460);
#9408=AXIS2_PLACEMENT_3D('',#15977,#11462,#11463);
#9409=AXIS2_PLACEMENT_3D('',#15979,#11464,#11465);
#9410=AXIS2_PLACEMENT_3D('',#15980,#11466,#11467);
#9411=AXIS2_PLACEMENT_3D('',#15982,#11468,#11469);
#9412=AXIS2_PLACEMENT_3D('',#15984,#11471,#11472);
#11403=DIRECTION('axis',(0.,0.,1.));
#11404=DIRECTION('refdir',(1.,0.,0.));
#11405=DIRECTION('center_axis',(0.866025403784439,0.,-0.5));
#11406=DIRECTION('ref_axis',(0.5,0.,0.866025403784439));
#11407=DIRECTION('',(-0.5,0.,-0.866025403784439));
#11408=DIRECTION('',(0.,-1.,0.));
#11409=DIRECTION('',(0.5,0.,0.866025403784439));
#11410=DIRECTION('',(0.,-1.,0.));
#11411=DIRECTION('center_axis',(1.60246890531964E-16,0.,-1.));
#11412=DIRECTION('ref_axis',(1.,0.,1.60246890531964E-16));
#11413=DIRECTION('',(-1.,0.,-1.60246890531964E-16));
#11414=DIRECTION('',(0.,-1.,0.));
#11415=DIRECTION('',(1.,0.,1.60246890531964E-16));
#11416=DIRECTION('center_axis',(-0.866025403784439,0.,-0.5));
#11417=DIRECTION('ref_axis',(0.5,0.,-0.866025403784439));
#11418=DIRECTION('',(-0.5,0.,0.866025403784439));
#11419=DIRECTION('',(0.,-1.,0.));
#11420=DIRECTION('',(0.5,0.,-0.866025403784439));
#11421=DIRECTION('center_axis',(-0.866025403784439,0.,0.5));
#11422=DIRECTION('ref_axis',(-0.5,0.,-0.866025403784439));
#11423=DIRECTION('',(0.5,0.,0.866025403784439));
#11424=DIRECTION('',(0.,-1.,0.));
#11425=DIRECTION('',(-0.5,0.,-0.866025403784439));
#11426=DIRECTION('center_axis',(-1.60246890531964E-16,0.,1.));
#11427=DIRECTION('ref_axis',(-1.,0.,-1.60246890531964E-16));
#11428=DIRECTION('',(1.,0.,1.60246890531964E-16));
#11429=DIRECTION('',(0.,-1.,0.));
#11430=DIRECTION('',(-1.,0.,-1.60246890531964E-16));
#11431=DIRECTION('center_axis',(0.866025403784439,0.,0.5));
#11432=DIRECTION('ref_axis',(-0.5,0.,0.866025403784439));
#11433=DIRECTION('',(0.5,0.,-0.866025403784439));
#11434=DIRECTION('',(-0.5,0.,0.866025403784439));
#11435=DIRECTION('center_axis',(0.,1.,0.));
#11436=DIRECTION('ref_axis',(1.,0.,0.));
#11437=DIRECTION('center_axis',(0.,-1.,0.));
#11438=DIRECTION('ref_axis',(0.,0.,-1.));
#11439=DIRECTION('center_axis',(0.,1.,0.));
#11440=DIRECTION('ref_axis',(1.,0.,0.));
#11441=DIRECTION('center_axis',(0.,1.,0.));
#11442=DIRECTION('ref_axis',(1.,0.,0.));
#11443=DIRECTION('center_axis',(0.,1.,0.));
#11444=DIRECTION('ref_axis',(0.,0.,1.));
#11445=DIRECTION('center_axis',(0.,-1.,0.));
#11446=DIRECTION('ref_axis',(1.,0.,0.));
#11447=DIRECTION('center_axis',(0.,-1.,0.));
#11448=DIRECTION('ref_axis',(1.,0.,0.));
#11449=DIRECTION('center_axis',(0.,-1.,0.));
#11450=DIRECTION('ref_axis',(1.,0.,0.));
#11451=DIRECTION('',(0.707106781186547,0.707106781186548,8.65956056235493E-17));
#11452=DIRECTION('center_axis',(0.,-1.,0.));
#11453=DIRECTION('ref_axis',(1.,0.,0.));
#11454=DIRECTION('center_axis',(0.,-1.,0.));
#11455=DIRECTION('ref_axis',(1.,0.,0.));
#11456=DIRECTION('',(0.,1.,0.));
#11457=DIRECTION('center_axis',(0.,1.,0.));
#11458=DIRECTION('ref_axis',(1.,0.,0.));
#11459=DIRECTION('center_axis',(0.,-1.,0.));
#11460=DIRECTION('ref_axis',(1.,0.,0.));
#11461=DIRECTION('',(-0.707106781186547,0.707106781186548,-8.65956056235493E-17));
#11462=DIRECTION('center_axis',(0.,-1.,0.));
#11463=DIRECTION('ref_axis',(0.,0.,-1.));
#11464=DIRECTION('center_axis',(0.,-1.,0.));
#11465=DIRECTION('ref_axis',(1.,0.,0.));
#11466=DIRECTION('center_axis',(0.,1.,0.));
#11467=DIRECTION('ref_axis',(1.,0.,0.));
#11468=DIRECTION('center_axis',(0.,1.,0.));
#11469=DIRECTION('ref_axis',(1.,0.,0.));
#11470=DIRECTION('',(-0.447213595499958,0.894427190999916,-5.47678698264203E-17));
#11471=DIRECTION('center_axis',(0.,-1.,0.));
#11472=DIRECTION('ref_axis',(1.,0.,0.));
#11473=DIRECTION('',(0.,1.,0.));
#15920=CARTESIAN_POINT('',(0.,0.,0.));
#15921=CARTESIAN_POINT('Origin',(0.0866025403784439,-0.4,-0.15));
#15922=CARTESIAN_POINT('',(0.173205080756888,-0.4,0.));
#15923=CARTESIAN_POINT('',(0.0866025403784439,-0.4,-0.15));
#15924=CARTESIAN_POINT('',(0.173205080756888,-0.4,0.));
#15925=CARTESIAN_POINT('',(0.0866025403784439,-0.64,-0.15));
#15926=CARTESIAN_POINT('',(0.0866025403784439,-0.4,-0.15));
#15927=CARTESIAN_POINT('',(0.173205080756888,-0.64,0.));
#15928=CARTESIAN_POINT('',(0.173205080756888,-0.64,0.));
#15929=CARTESIAN_POINT('',(0.173205080756888,-0.4,0.));
#15930=CARTESIAN_POINT('Origin',(-0.0866025403784438,-0.4,-0.15));
#15931=CARTESIAN_POINT('',(-0.0866025403784438,-0.4,-0.15));
#15932=CARTESIAN_POINT('',(0.0866025403784439,-0.4,-0.15));
#15933=CARTESIAN_POINT('',(-0.0866025403784438,-0.64,-0.15));
#15934=CARTESIAN_POINT('',(-0.0866025403784438,-0.4,-0.15));
#15935=CARTESIAN_POINT('',(0.0866025403784439,-0.64,-0.15));
#15936=CARTESIAN_POINT('Origin',(-0.173205080756888,-0.4,-2.77555756156289E-17));
#15937=CARTESIAN_POINT('',(-0.173205080756888,-0.4,-2.12115047744981E-17));
#15938=CARTESIAN_POINT('',(-0.0866025403784438,-0.4,-0.15));
#15939=CARTESIAN_POINT('',(-0.173205080756888,-0.64,-2.77555756156289E-17));
#15940=CARTESIAN_POINT('',(-0.173205080756888,-0.4,-2.12115047744981E-17));
#15941=CARTESIAN_POINT('',(-0.0866025403784438,-0.64,-0.15));
#15942=CARTESIAN_POINT('Origin',(-0.0866025403784439,-0.4,0.15));
#15943=CARTESIAN_POINT('',(-0.0866025403784439,-0.4,0.15));
#15944=CARTESIAN_POINT('',(-0.173205080756888,-0.4,-2.12115047744981E-17));
#15945=CARTESIAN_POINT('',(-0.0866025403784439,-0.64,0.15));
#15946=CARTESIAN_POINT('',(-0.0866025403784439,-0.4,0.15));
#15947=CARTESIAN_POINT('',(-0.173205080756888,-0.64,-2.12115047744981E-17));
#15948=CARTESIAN_POINT('Origin',(0.0866025403784439,-0.4,0.15));
#15949=CARTESIAN_POINT('',(0.0866025403784439,-0.4,0.15));
#15950=CARTESIAN_POINT('',(-0.0866025403784439,-0.4,0.15));
#15951=CARTESIAN_POINT('',(0.0866025403784439,-0.64,0.15));
#15952=CARTESIAN_POINT('',(0.0866025403784439,-0.4,0.15));
#15953=CARTESIAN_POINT('',(-0.0866025403784439,-0.64,0.15));
#15954=CARTESIAN_POINT('Origin',(0.173205080756888,-0.4,0.));
#15955=CARTESIAN_POINT('',(0.0866025403784439,-0.4,0.15));
#15956=CARTESIAN_POINT('',(0.0866025403784439,-0.64,0.15));
#15957=CARTESIAN_POINT('Origin',(0.,-0.4,-2.77555756156289E-17));
#15958=CARTESIAN_POINT('Origin',(0.,-0.64,-2.77555756156289E-17));
#15959=CARTESIAN_POINT('Origin',(0.,-1.,0.));
#15960=CARTESIAN_POINT('',(-0.1954,-1.,2.39295984553393E-17));
#15961=CARTESIAN_POINT('Origin',(0.,-1.,0.));
#15962=CARTESIAN_POINT('Origin',(0.3,0.4,0.));
#15963=CARTESIAN_POINT('',(-0.3,0.4,-3.67394039744206E-17));
#15964=CARTESIAN_POINT('Origin',(0.,0.4,0.));
#15965=CARTESIAN_POINT('Origin',(0.,0.375,0.));
#15966=CARTESIAN_POINT('',(-0.35,0.35,-4.28626379701573E-17));
#15967=CARTESIAN_POINT('Origin',(0.,0.35,0.));
#15968=CARTESIAN_POINT('',(-0.325,0.375,-3.9801020972289E-17));
#15969=CARTESIAN_POINT('Origin',(0.,0.19,0.));
#15970=CARTESIAN_POINT('',(-0.35,0.03,-4.28626379701574E-17));
#15971=CARTESIAN_POINT('Origin',(0.,0.03,0.));
#15972=CARTESIAN_POINT('',(-0.35,0.19,-4.28626379701574E-17));
#15973=CARTESIAN_POINT('Origin',(0.,0.0149999999999999,0.));
#15974=CARTESIAN_POINT('',(-0.32,-3.29597460435593E-17,-3.91886975727153E-17));
#15975=CARTESIAN_POINT('Origin',(0.,0.,0.));
#15976=CARTESIAN_POINT('',(-0.335,0.0149999999999999,-4.10256677714363E-17));
#15977=CARTESIAN_POINT('Origin',(0.22,0.,0.));
#15978=CARTESIAN_POINT('',(-0.22,-6.93889390390723E-18,-2.69422295812418E-17));
#15979=CARTESIAN_POINT('Origin',(0.,0.,0.));
#15980=CARTESIAN_POINT('Origin',(0.,-0.02,0.));
#15981=CARTESIAN_POINT('',(-0.1954,-0.0492,2.39295984553393E-17));
#15982=CARTESIAN_POINT('Origin',(0.,-0.0492,0.));
#15983=CARTESIAN_POINT('',(-0.21,-0.02,-2.57175827820944E-17));
#15984=CARTESIAN_POINT('Origin',(0.,-0.8,0.));
#15985=CARTESIAN_POINT('',(-0.1954,-0.8,-2.39295984553393E-17));
#16973=UNCERTAINTY_MEASURE_WITH_UNIT(LENGTH_MEASURE(0.001),#17047,
'DISTANCE_ACCURACY_VALUE',
'Maximum model space distance between geometric entities at asserted c
onnectivities');
#16993=UNCERTAINTY_MEASURE_WITH_UNIT(LENGTH_MEASURE(0.001),#17047,
'DISTANCE_ACCURACY_VALUE',
'Maximum model space distance between geometric entities at asserted c
onnectivities');
#17026=(
GEOMETRIC_REPRESENTATION_CONTEXT(3)
GLOBAL_UNCERTAINTY_ASSIGNED_CONTEXT((#16973))
GLOBAL_UNIT_ASSIGNED_CONTEXT((#17047,#17049,#17050))
REPRESENTATION_CONTEXT('','3D')
);
#17046=(
GEOMETRIC_REPRESENTATION_CONTEXT(3)
GLOBAL_UNCERTAINTY_ASSIGNED_CONTEXT((#16993))
GLOBAL_UNIT_ASSIGNED_CONTEXT((#17047,#17049,#17050))
REPRESENTATION_CONTEXT('','3D')
);
#17047=(
LENGTH_UNIT()
NAMED_UNIT(*)
SI_UNIT(.CENTI.,.METRE.)
);
#17049=(
NAMED_UNIT(*)
PLANE_ANGLE_UNIT()
SI_UNIT($,.RADIAN.)
);
#17050=(
NAMED_UNIT(*)
SI_UNIT($,.STERADIAN.)
SOLID_ANGLE_UNIT()
);
#17083=SHAPE_DEFINITION_REPRESENTATION(#17140,#17290);
#17140=PRODUCT_DEFINITION_SHAPE('',$,#17343);
#17290=SHAPE_REPRESENTATION('',(#9389),#17026);
#17310=PRODUCT_DEFINITION_CONTEXT('part definition',#17468,'design');
#17343=PRODUCT_DEFINITION('M4x10 Cap Screw','M4x10 Cap Screw',#17395,#17310);
#17395=PRODUCT_DEFINITION_FORMATION('',$,#17502);
#17468=APPLICATION_CONTEXT(
'Core Data for Automotive Mechanical Design Process');
#17469=PRODUCT_CONTEXT('part definition',#17468,'mechanical');
#17502=PRODUCT('M4x10 Cap Screw','M4x10 Cap Screw','M4x10 Cap Screw',(#17469));
#17592=COLOUR_RGB('Black',0.12,0.14,0.17);
#17593=FILL_AREA_STYLE_COLOUR('',#17592);
#17594=FILL_AREA_STYLE('',(#17593));
#17595=SURFACE_STYLE_FILL_AREA(#17594);
#17596=SURFACE_SIDE_STYLE('',(#17595));
#17597=SURFACE_STYLE_USAGE(.BOTH.,#17596);
#17598=PRESENTATION_STYLE_ASSIGNMENT((#17597));
ENDSEC;
END-ISO-10303-21;
